ISO-10303-21;
HEADER;
FILE_DESCRIPTION (('STEP AP214'),
    '1' );
FILE_NAME ('o-rings series a_iso_O-ring 4x1.8-A-ISO 3601-1.step',
    '2026-10-24T08:20:21',
    ( '' ),
    ( '' ),
    'SwSTEP 2.0',
    'SolidWorks 2026',
    '' );
FILE_SCHEMA (( 'AUTOMOTIVE_DESIGN' ));
ENDSEC;

DATA;
#2=DIRECTION ( 'NONE',  ( -1.000000000000000000, 0.000000000000000000, 0.000000000000000000 ) ) ;
#17=DIRECTION ( 'NONE',  ( -1.000000000000000000, -1.224646799147353454E-16, 0.000000000000000000 ) ) ;
#46=EDGE_CURVE ( 'NONE', #2758, #1577, #1662, .T. ) ;
#54=ORIENTED_EDGE ( 'NONE', *, *, #3614, .T. ) ;
#96=ORIENTED_EDGE ( 'NONE', *, *, #3202, .F. ) ;
#99=ADVANCED_FACE ( 'NONE', ( #3496 ), #810, .T. ) ;
#153=COLOUR_RGB ( '',1.000000000000000000, 0.9490196078431372140, 0.9098039215686274384 ) ;
#218=ORIENTED_EDGE ( 'NONE', *, *, #3772, .F. ) ;
#220=PRODUCT_DEFINITION_FORMATION_WITH_SPECIFIED_SOURCE ( 'ANY', '', #2168, .NOT_KNOWN. ) ;
#227=DIRECTION ( 'NONE',  ( -0.000000000000000000, -0.000000000000000000, -1.000000000000000000 ) ) ;
#274=ORIENTED_EDGE ( 'NONE', *, *, #2686, .T. ) ;
#275=EDGE_CURVE ( 'NONE', #1577, #1374, #3092, .T. ) ;
#282=SHAPE_REPRESENTATION ( 'o-rings series a_iso_O-ring 4x1.8-A-ISO 3601-1', ( #2207 ), #2896 ) ;
#287=PRESENTATION_STYLE_ASSIGNMENT (( #2918 ) ) ;
#289=ORIENTED_EDGE ( 'NONE', *, *, #46, .F. ) ;
#306=EDGE_LOOP ( 'NONE', ( #2682, #2580, #1353, #1330 ) ) ;
#353=ORIENTED_EDGE ( 'NONE', *, *, #1947, .T. ) ;
#364=EDGE_LOOP ( 'NONE', ( #96, #54, #353, #289 ) ) ;
#449=CIRCLE ( 'NONE', #3007, 3.799999999999999378 ) ;
#460=( NAMED_UNIT ( * ) PLANE_ANGLE_UNIT ( ) SI_UNIT ( $, .RADIAN. ) );
#471=DIRECTION ( 'NONE',  ( -1.000000000000000000, 0.000000000000000000, 0.000000000000000000 ) ) ;
#475=EDGE_LOOP ( 'NONE', ( #2661, #3268, #2052, #1054 ) ) ;
#477=PRODUCT_DEFINITION_CONTEXT ( 'detailed design', #626, 'design' ) ;
#487=CARTESIAN_POINT ( 'NONE',  ( 3.799999999999999378, 4.653657836759941744E-16, 0.000000000000000000 ) ) ;
#498=DIRECTION ( 'NONE',  ( -1.000000000000000000, 0.000000000000000000, 0.000000000000000000 ) ) ;
#520=CARTESIAN_POINT ( 'NONE',  ( 0.000000000000000000, 0.000000000000000000, 0.000000000000000000 ) ) ;
#572=( NAMED_UNIT ( * ) PLANE_ANGLE_UNIT ( ) SI_UNIT ( $, .RADIAN. ) );
#609=DIRECTION ( 'NONE',  ( -0.000000000000000000, -0.000000000000000000, -1.000000000000000000 ) ) ;
#615=CLOSED_SHELL ( 'NONE', ( #99, #3472, #2462, #648 ) ) ;
#618=DIRECTION ( 'NONE',  ( -1.224646799147353207E-16, 1.000000000000000000, 0.000000000000000000 ) ) ;
#626=APPLICATION_CONTEXT ( 'automotive_design' ) ;
#648=ADVANCED_FACE ( 'NONE', ( #1170 ), #1153, .T. ) ;
#660=UNCERTAINTY_MEASURE_WITH_UNIT (LENGTH_MEASURE( 1.000000000000000082E-05 ), #3741, 'distance_accuracy_value', 'NONE');
#810=TOROIDAL_SURFACE ( 'NONE', #1437, 2.899999999999999911, 0.8999999999999999112 ) ;
#820=CARTESIAN_POINT ( 'NONE',  ( 0.000000000000000000, 0.000000000000000000, 0.000000000000000000 ) ) ;
#840=CIRCLE ( 'NONE', #3141, 0.8999999999999999112 ) ;
#902=DIRECTION ( 'NONE',  ( -0.000000000000000000, -0.000000000000000000, -1.000000000000000000 ) ) ;
#936=DIRECTION ( 'NONE',  ( -1.000000000000000000, 0.000000000000000000, 0.000000000000000000 ) ) ;
#960=STYLED_ITEM('',(#3881),#3213);
#994=PRODUCT_DEFINITION_SHAPE ( 'NONE', 'NONE',  #2395 ) ;
#998=CARTESIAN_POINT ( 'NONE',  ( -3.799999999999999378, 0.000000000000000000, 0.000000000000000000 ) ) ;
#1039=FILL_AREA_STYLE_COLOUR ( '', #153 ) ;
#1054=ORIENTED_EDGE ( 'NONE', *, *, #275, .T. ) ;
#1059=DIRECTION ( 'NONE',  ( -0.000000000000000000, -0.000000000000000000, -1.000000000000000000 ) ) ;
#1087=CIRCLE ( 'NONE', #2509, 0.8999999999999999112 ) ;
#1097=CIRCLE ( 'NONE', #3701, 3.799999999999999378 ) ;
#1150=SURFACE_STYLE_FILL_AREA ( #3582 ) ;
#1153=TOROIDAL_SURFACE ( 'NONE', #2523, 2.899999999999999911, 0.8999999999999999112 ) ;
#1154=( GEOMETRIC_REPRESENTATION_CONTEXT ( 3 ) GLOBAL_UNCERTAINTY_ASSIGNED_CONTEXT ( ( #1916 ) ) GLOBAL_UNIT_ASSIGNED_CONTEXT ( ( #2623, #1473, #3811 ) ) REPRESENTATION_CONTEXT ( 'NONE', 'WORKASPACE' ) );
#1170=FACE_OUTER_BOUND ( 'NONE', #2696, .T. ) ;
#1173=FACE_OUTER_BOUND ( 'NONE', #364, .T. ) ;
#1196=CARTESIAN_POINT ( 'NONE',  ( 0.000000000000000000, 0.000000000000000000, 0.000000000000000000 ) ) ;
#1238=VERTEX_POINT ( 'NONE', #998 ) ;
#1242=CARTESIAN_POINT ( 'NONE',  ( 0.000000000000000000, 0.000000000000000000, 1.102182119232617788E-16 ) ) ;
#1269=( GEOMETRIC_REPRESENTATION_CONTEXT ( 3 ) GLOBAL_UNCERTAINTY_ASSIGNED_CONTEXT ( ( #3501 ) ) GLOBAL_UNIT_ASSIGNED_CONTEXT ( ( #2407, #572, #1760 ) ) REPRESENTATION_CONTEXT ( 'NONE', 'WORKASPACE' ) );
#1330=ORIENTED_EDGE ( 'NONE', *, *, #2686, .F. ) ;
#1353=ORIENTED_EDGE ( 'NONE', *, *, #3202, .T. ) ;
#1374=VERTEX_POINT ( 'NONE', #487 ) ;
#1437=AXIS2_PLACEMENT_3D ( 'NONE', #520, #227, #498 ) ;
#1446=CIRCLE ( 'NONE', #3012, 2.000000000000000000 ) ;
#1449=PRODUCT_CONTEXT ( 'NONE', #1892, 'mechanical' ) ;
#1473=( NAMED_UNIT ( * ) PLANE_ANGLE_UNIT ( ) SI_UNIT ( $, .RADIAN. ) );
#1522=MECHANICAL_DESIGN_GEOMETRIC_PRESENTATION_REPRESENTATION('',(#2963),#1154);
#1554=CARTESIAN_POINT ( 'NONE',  ( 0.000000000000000000, 0.000000000000000000, 0.000000000000000000 ) ) ;
#1572=ADVANCED_BREP_SHAPE_REPRESENTATION ( '', ( #3213, #2207 ), #2896 ) ;
#1577=VERTEX_POINT ( 'NONE', #3230 ) ;
#1637=MECHANICAL_DESIGN_GEOMETRIC_PRESENTATION_REPRESENTATION('',(#960),#1269);
#1661=DIRECTION ( 'NONE',  ( -0.000000000000000000, -0.000000000000000000, -1.000000000000000000 ) ) ;
#1662=CIRCLE ( 'NONE', #3545, 2.000000000000000000 ) ;
#1754=CARTESIAN_POINT ( 'NONE',  ( 0.000000000000000000, 0.000000000000000000, 0.000000000000000000 ) ) ;
#1760=( NAMED_UNIT ( * ) SI_UNIT ( $, .STERADIAN. ) SOLID_ANGLE_UNIT ( ) );
#1812=CARTESIAN_POINT ( 'NONE',  ( 0.000000000000000000, 0.000000000000000000, 0.000000000000000000 ) ) ;
#1855=DIRECTION ( 'NONE',  ( -1.000000000000000000, 0.000000000000000000, 0.000000000000000000 ) ) ;
#1886=DIRECTION ( 'NONE',  ( -1.000000000000000000, 0.000000000000000000, 0.000000000000000000 ) ) ;
#1892=APPLICATION_CONTEXT ( 'automotive_design' ) ;
#1916=UNCERTAINTY_MEASURE_WITH_UNIT (LENGTH_MEASURE( 1.000000000000000082E-05 ), #2623, 'distance_accuracy_value', 'NONE');
#1933=CARTESIAN_POINT ( 'NONE',  ( -2.899999999999999911, 0.000000000000000000, 0.000000000000000000 ) ) ;
#1947=EDGE_CURVE ( 'NONE', #1374, #1577, #2321, .T. ) ;
#2052=ORIENTED_EDGE ( 'NONE', *, *, #46, .T. ) ;
#2075=DIRECTION ( 'NONE',  ( 0.000000000000000000, -1.000000000000000000, 0.000000000000000000 ) ) ;
#2113=DIRECTION ( 'NONE',  ( -0.000000000000000000, -0.000000000000000000, -1.000000000000000000 ) ) ;
#2168=PRODUCT ( 'o-rings series a_iso_O-ring 4x1.8-A-ISO 3601-1', 'o-rings series a_iso_O-ring 4x1.8-A-ISO 3601-1', '', ( #1449 ) ) ;
#2169=DIRECTION ( 'NONE',  ( 0.000000000000000000, 0.000000000000000000, -1.000000000000000000 ) ) ;
#2207=AXIS2_PLACEMENT_3D ( 'NONE', #820, #2246, #3194 ) ;
#2241=DIRECTION ( 'NONE',  ( -1.000000000000000000, 0.000000000000000000, 0.000000000000000000 ) ) ;
#2246=DIRECTION ( 'NONE',  ( 0.000000000000000000, 0.000000000000000000, 1.000000000000000000 ) ) ;
#2321=CIRCLE ( 'NONE', #3750, 0.8999999999999998002 ) ;
#2357=CARTESIAN_POINT ( 'NONE',  ( 2.899999999999999911, 3.551475717527323832E-16, 0.000000000000000000 ) ) ;
#2380=DIRECTION ( 'NONE',  ( -0.000000000000000000, -0.000000000000000000, -1.000000000000000000 ) ) ;
#2395=PRODUCT_DEFINITION ( 'UNKNOWN', '', #220, #477 ) ;
#2407=( LENGTH_UNIT ( ) NAMED_UNIT ( * ) SI_UNIT ( .MILLI., .METRE. ) );
#2439=FACE_OUTER_BOUND ( 'NONE', #475, .T. ) ;
#2444=CARTESIAN_POINT ( 'NONE',  ( -2.000000000000000000, 0.000000000000000000, 1.102182119232618034E-16 ) ) ;
#2462=ADVANCED_FACE ( 'NONE', ( #2439 ), #2572, .T. ) ;
#2509=AXIS2_PLACEMENT_3D ( 'NONE', #3279, #2075, #3257 ) ;
#2523=AXIS2_PLACEMENT_3D ( 'NONE', #2941, #902, #936 ) ;
#2572=TOROIDAL_SURFACE ( 'NONE', #2945, 2.899999999999999911, 0.8999999999999999112 ) ;
#2580=ORIENTED_EDGE ( 'NONE', *, *, #3772, .T. ) ;
#2622=DIRECTION ( 'NONE',  ( -1.000000000000000000, -1.224646799147353454E-16, 0.000000000000000000 ) ) ;
#2623=( LENGTH_UNIT ( ) NAMED_UNIT ( * ) SI_UNIT ( .MILLI., .METRE. ) );
#2661=ORIENTED_EDGE ( 'NONE', *, *, #3614, .F. ) ;
#2670=SHAPE_REPRESENTATION_RELATIONSHIP ( 'NONE' , 'NONE' ,  #282, #1572 ) ;
#2682=ORIENTED_EDGE ( 'NONE', *, *, #1947, .F. ) ;
#2686=EDGE_CURVE ( 'NONE', #1577, #2758, #1446, .T. ) ;
#2696=EDGE_LOOP ( 'NONE', ( #218, #3406, #274, #3520 ) ) ;
#2725=CARTESIAN_POINT ( 'NONE',  ( 2.899999999999999911, 3.551475717527323832E-16, 0.000000000000000000 ) ) ;
#2758=VERTEX_POINT ( 'NONE', #2444 ) ;
#2800=SHAPE_DEFINITION_REPRESENTATION ( #994, #282 ) ;
#2844=( NAMED_UNIT ( * ) SI_UNIT ( $, .STERADIAN. ) SOLID_ANGLE_UNIT ( ) );
#2896=( GEOMETRIC_REPRESENTATION_CONTEXT ( 3 ) GLOBAL_UNCERTAINTY_ASSIGNED_CONTEXT ( ( #660 ) ) GLOBAL_UNIT_ASSIGNED_CONTEXT ( ( #3741, #460, #2844 ) ) REPRESENTATION_CONTEXT ( 'NONE', 'WORKASPACE' ) );
#2918=SURFACE_STYLE_USAGE ( .BOTH. , #2962 ) ;
#2941=CARTESIAN_POINT ( 'NONE',  ( 0.000000000000000000, 0.000000000000000000, 0.000000000000000000 ) ) ;
#2945=AXIS2_PLACEMENT_3D ( 'NONE', #1196, #2113, #1855 ) ;
#2962=SURFACE_SIDE_STYLE ('',( #1150 ) ) ;
#2963=STYLED_ITEM ( 'NONE', ( #287 ), #1572 ) ;
#2969=EDGE_CURVE ( 'NONE', #2758, #1238, #840, .T. ) ;
#2978=DIRECTION ( 'NONE',  ( -0.000000000000000000, -0.000000000000000000, -1.000000000000000000 ) ) ;
#2986=DIRECTION ( 'NONE',  ( -1.000000000000000000, 0.000000000000000000, 0.000000000000000000 ) ) ;
#3003=TOROIDAL_SURFACE ( 'NONE', #3493, 2.899999999999999911, 0.8999999999999999112 ) ;
#3007=AXIS2_PLACEMENT_3D ( 'NONE', #1754, #2380, #1886 ) ;
#3012=AXIS2_PLACEMENT_3D ( 'NONE', #1242, #2978, #2 ) ;
#3092=CIRCLE ( 'NONE', #3260, 0.8999999999999998002 ) ;
#3129=DIRECTION ( 'NONE',  ( 0.000000000000000000, -1.000000000000000000, 0.000000000000000000 ) ) ;
#3141=AXIS2_PLACEMENT_3D ( 'NONE', #1933, #3129, #2169 ) ;
#3194=DIRECTION ( 'NONE',  ( 1.000000000000000000, 0.000000000000000000, 0.000000000000000000 ) ) ;
#3202=EDGE_CURVE ( 'NONE', #1238, #2758, #1087, .T. ) ;
#3213=MANIFOLD_SOLID_BREP ( 'Sweep1', #615 ) ;
#3230=CARTESIAN_POINT ( 'NONE',  ( 2.000000000000000000, 2.449293598294706414E-16, 0.000000000000000000 ) ) ;
#3257=DIRECTION ( 'NONE',  ( 0.000000000000000000, 0.000000000000000000, -1.000000000000000000 ) ) ;
#3260=AXIS2_PLACEMENT_3D ( 'NONE', #2725, #618, #17 ) ;
#3268=ORIENTED_EDGE ( 'NONE', *, *, #2969, .F. ) ;
#3279=CARTESIAN_POINT ( 'NONE',  ( -2.899999999999999911, 0.000000000000000000, 0.000000000000000000 ) ) ;
#3406=ORIENTED_EDGE ( 'NONE', *, *, #275, .F. ) ;
#3472=ADVANCED_FACE ( 'NONE', ( #1173 ), #3003, .T. ) ;
#3493=AXIS2_PLACEMENT_3D ( 'NONE', #1812, #609, #2986 ) ;
#3496=FACE_OUTER_BOUND ( 'NONE', #306, .T. ) ;
#3501=UNCERTAINTY_MEASURE_WITH_UNIT (LENGTH_MEASURE( 1.000000000000000082E-05 ), #2407, 'distance_accuracy_value', 'NONE');
#3520=ORIENTED_EDGE ( 'NONE', *, *, #2969, .T. ) ;
#3545=AXIS2_PLACEMENT_3D ( 'NONE', #3719, #1059, #2241 ) ;
#3582=FILL_AREA_STYLE ('',( #1039 ) ) ;
#3614=EDGE_CURVE ( 'NONE', #1238, #1374, #449, .T. ) ;
#3701=AXIS2_PLACEMENT_3D ( 'NONE', #1554, #1661, #471 ) ;
#3719=CARTESIAN_POINT ( 'NONE',  ( 0.000000000000000000, 0.000000000000000000, 1.102182119232617788E-16 ) ) ;
#3741=( LENGTH_UNIT ( ) NAMED_UNIT ( * ) SI_UNIT ( .MILLI., .METRE. ) );
#3750=AXIS2_PLACEMENT_3D ( 'NONE', #2357, #3810, #2622 ) ;
#3772=EDGE_CURVE ( 'NONE', #1374, #1238, #1097, .T. ) ;
#3810=DIRECTION ( 'NONE',  ( -1.224646799147353207E-16, 1.000000000000000000, 0.000000000000000000 ) ) ;
#3811=( NAMED_UNIT ( * ) SI_UNIT ( $, .STERADIAN. ) SOLID_ANGLE_UNIT ( ) );
#3875=COLOUR_RGB('Black',0.12,0.14,0.17);
#3876=FILL_AREA_STYLE_COLOUR('',#3875);
#3877=FILL_AREA_STYLE('',(#3876));
#3878=SURFACE_STYLE_FILL_AREA(#3877);
#3879=SURFACE_SIDE_STYLE('',(#3878));
#3880=SURFACE_STYLE_USAGE(.BOTH.,#3879);
#3881=PRESENTATION_STYLE_ASSIGNMENT((#3880));
ENDSEC;
END-ISO-10303-21;
